ISO-10303-21;
HEADER;
/* Generated by software containing ST-Developer
 * from STEP Tools, Inc. (www.steptools.com) 
 */

FILE_DESCRIPTION(
/* description */ ('Hand wheel with handle and shaft collar'),
/* implementation_level */ '2;1');

FILE_NAME(
/* name */ 'Outer ring (1).step',
/* time_stamp */ '2026-10-28T03:23:19-07:00',
/* author */ (''),
/* organization */ (''),
/* preprocessor_version */ 'ST-DEVELOPER v20.2',
/* originating_system */ 'Autodesk Translation Framework v15.17.0.0',
/* authorisation */ '');

FILE_SCHEMA (('AUTOMOTIVE_DESIGN { 1 0 10303 214 3 1 1 }'));
ENDSEC;

DATA;
#10=MECHANICAL_DESIGN_GEOMETRIC_PRESENTATION_REPRESENTATION('',(#427),#10510);
#300=TOROIDAL_SURFACE('',#6214,1.,0.247676);
#319=CONICAL_SURFACE('',#6225,1.47,0.785398163397449);
#320=CONICAL_SURFACE('',#6229,1.47,0.785398163397449);
#356=SHAPE_REPRESENTATION_RELATIONSHIP('SRR','None',#10675,#388);
#388=ADVANCED_BREP_SHAPE_REPRESENTATION('',(#472),#10502);
#427=STYLED_ITEM('',(#10908),#472);
#472=MANIFOLD_SOLID_BREP('Body1',#5328);
#585=FACE_BOUND('',#1433,.T.);
#586=FACE_BOUND('',#1438,.T.);
#732=PLANE('',#6222);
#733=PLANE('',#6231);
#1012=FACE_OUTER_BOUND('',#1430,.T.);
#1013=FACE_OUTER_BOUND('',#1431,.T.);
#1014=FACE_OUTER_BOUND('',#1432,.T.);
#1015=FACE_OUTER_BOUND('',#1434,.T.);
#1016=FACE_OUTER_BOUND('',#1435,.T.);
#1017=FACE_OUTER_BOUND('',#1436,.T.);
#1018=FACE_OUTER_BOUND('',#1437,.T.);
#1019=FACE_OUTER_BOUND('',#1439,.T.);
#1430=EDGE_LOOP('',(#4605,#4606,#4607,#4608,#4609,#4610));
#1431=EDGE_LOOP('',(#4611,#4612,#4613,#4614,#4615));
#1432=EDGE_LOOP('',(#4616));
#1433=EDGE_LOOP('',(#4617));
#1434=EDGE_LOOP('',(#4618,#4619,#4620,#4621));
#1435=EDGE_LOOP('',(#4622,#4623,#4624,#4625));
#1436=EDGE_LOOP('',(#4626,#4627,#4628,#4629));
#1437=EDGE_LOOP('',(#4630));
#1438=EDGE_LOOP('',(#4631));
#1439=EDGE_LOOP('',(#4632,#4633,#4634,#4635,#4636));
#1783=LINE('',#9745,#2093);
#1784=LINE('',#9754,#2094);
#1785=LINE('',#9758,#2095);
#1786=LINE('',#9762,#2096);
#1787=LINE('',#9765,#2097);
#2093=VECTOR('',#7739,1.023815);
#2094=VECTOR('',#7750,1.47);
#2095=VECTOR('',#7755,1.5);
#2096=VECTOR('',#7760,1.47);
#2097=VECTOR('',#7765,1.023815);
#2365=CIRCLE('',#6215,1.023815);
#2366=CIRCLE('',#6216,1.023815);
#2367=CIRCLE('',#6217,0.247676);
#2368=CIRCLE('',#6218,1.023815);
#2369=CIRCLE('',#6219,1.023815);
#2370=CIRCLE('',#6221,1.023815);
#2371=CIRCLE('',#6223,1.44);
#2372=CIRCLE('',#6224,1.023815);
#2373=CIRCLE('',#6226,1.5);
#2374=CIRCLE('',#6228,1.5);
#2375=CIRCLE('',#6230,1.44);
#2796=VERTEX_POINT('',#9733);
#2797=VERTEX_POINT('',#9734);
#2798=VERTEX_POINT('',#9737);
#2799=VERTEX_POINT('',#9739);
#2800=VERTEX_POINT('',#9743);
#2801=VERTEX_POINT('',#9747);
#2802=VERTEX_POINT('',#9749);
#2803=VERTEX_POINT('',#9752);
#2804=VERTEX_POINT('',#9756);
#2805=VERTEX_POINT('',#9760);
#3420=EDGE_CURVE('',#2796,#2797,#2365,.T.);
#3421=EDGE_CURVE('',#2797,#2796,#2366,.T.);
#3422=EDGE_CURVE('',#2797,#2798,#2367,.T.);
#3423=EDGE_CURVE('',#2799,#2798,#2368,.T.);
#3424=EDGE_CURVE('',#2798,#2799,#2369,.T.);
#3425=EDGE_CURVE('',#2800,#2800,#2370,.T.);
#3426=EDGE_CURVE('',#2800,#2799,#1783,.T.);
#3427=EDGE_CURVE('',#2801,#2801,#2371,.T.);
#3428=EDGE_CURVE('',#2802,#2802,#2372,.T.);
#3429=EDGE_CURVE('',#2803,#2803,#2373,.T.);
#3430=EDGE_CURVE('',#2803,#2801,#1784,.T.);
#3431=EDGE_CURVE('',#2804,#2804,#2374,.T.);
#3432=EDGE_CURVE('',#2804,#2803,#1785,.T.);
#3433=EDGE_CURVE('',#2805,#2805,#2375,.T.);
#3434=EDGE_CURVE('',#2805,#2804,#1786,.T.);
#3435=EDGE_CURVE('',#2796,#2802,#1787,.T.);
#4605=ORIENTED_EDGE('',*,*,#3420,.F.);
#4606=ORIENTED_EDGE('',*,*,#3421,.F.);
#4607=ORIENTED_EDGE('',*,*,#3422,.T.);
#4608=ORIENTED_EDGE('',*,*,#3423,.F.);
#4609=ORIENTED_EDGE('',*,*,#3424,.F.);
#4610=ORIENTED_EDGE('',*,*,#3422,.F.);
#4611=ORIENTED_EDGE('',*,*,#3425,.T.);
#4612=ORIENTED_EDGE('',*,*,#3426,.T.);
#4613=ORIENTED_EDGE('',*,*,#3423,.T.);
#4614=ORIENTED_EDGE('',*,*,#3424,.T.);
#4615=ORIENTED_EDGE('',*,*,#3426,.F.);
#4616=ORIENTED_EDGE('',*,*,#3427,.F.);
#4617=ORIENTED_EDGE('',*,*,#3428,.T.);
#4618=ORIENTED_EDGE('',*,*,#3429,.F.);
#4619=ORIENTED_EDGE('',*,*,#3430,.T.);
#4620=ORIENTED_EDGE('',*,*,#3427,.T.);
#4621=ORIENTED_EDGE('',*,*,#3430,.F.);
#4622=ORIENTED_EDGE('',*,*,#3431,.F.);
#4623=ORIENTED_EDGE('',*,*,#3432,.T.);
#4624=ORIENTED_EDGE('',*,*,#3429,.T.);
#4625=ORIENTED_EDGE('',*,*,#3432,.F.);
#4626=ORIENTED_EDGE('',*,*,#3433,.F.);
#4627=ORIENTED_EDGE('',*,*,#3434,.T.);
#4628=ORIENTED_EDGE('',*,*,#3431,.T.);
#4629=ORIENTED_EDGE('',*,*,#3434,.F.);
#4630=ORIENTED_EDGE('',*,*,#3433,.T.);
#4631=ORIENTED_EDGE('',*,*,#3425,.F.);
#4632=ORIENTED_EDGE('',*,*,#3420,.T.);
#4633=ORIENTED_EDGE('',*,*,#3421,.T.);
#4634=ORIENTED_EDGE('',*,*,#3435,.T.);
#4635=ORIENTED_EDGE('',*,*,#3428,.F.);
#4636=ORIENTED_EDGE('',*,*,#3435,.F.);
#4959=CYLINDRICAL_SURFACE('',#6220,1.023815);
#4960=CYLINDRICAL_SURFACE('',#6227,1.5);
#4961=CYLINDRICAL_SURFACE('',#6232,1.023815);
#5224=ADVANCED_FACE('',(#1012),#300,.F.);
#5225=ADVANCED_FACE('',(#1013),#4959,.F.);
#5226=ADVANCED_FACE('',(#1014,#585),#732,.T.);
#5227=ADVANCED_FACE('',(#1015),#319,.T.);
#5228=ADVANCED_FACE('',(#1016),#4960,.T.);
#5229=ADVANCED_FACE('',(#1017),#320,.T.);
#5230=ADVANCED_FACE('',(#1018,#586),#733,.T.);
#5231=ADVANCED_FACE('',(#1019),#4961,.F.);
#5328=CLOSED_SHELL('',(#5224,#5225,#5226,#5227,#5228,#5229,#5230,#5231));
#6213=AXIS2_PLACEMENT_3D('',#9731,#7721,#7722);
#6214=AXIS2_PLACEMENT_3D('',#9732,#7723,#7724);
#6215=AXIS2_PLACEMENT_3D('',#9735,#7725,#7726);
#6216=AXIS2_PLACEMENT_3D('',#9736,#7727,#7728);
#6217=AXIS2_PLACEMENT_3D('',#9738,#7729,#7730);
#6218=AXIS2_PLACEMENT_3D('',#9740,#7731,#7732);
#6219=AXIS2_PLACEMENT_3D('',#9741,#7733,#7734);
#6220=AXIS2_PLACEMENT_3D('',#9742,#7735,#7736);
#6221=AXIS2_PLACEMENT_3D('',#9744,#7737,#7738);
#6222=AXIS2_PLACEMENT_3D('',#9746,#7740,#7741);
#6223=AXIS2_PLACEMENT_3D('',#9748,#7742,#7743);
#6224=AXIS2_PLACEMENT_3D('',#9750,#7744,#7745);
#6225=AXIS2_PLACEMENT_3D('',#9751,#7746,#7747);
#6226=AXIS2_PLACEMENT_3D('',#9753,#7748,#7749);
#6227=AXIS2_PLACEMENT_3D('',#9755,#7751,#7752);
#6228=AXIS2_PLACEMENT_3D('',#9757,#7753,#7754);
#6229=AXIS2_PLACEMENT_3D('',#9759,#7756,#7757);
#6230=AXIS2_PLACEMENT_3D('',#9761,#7758,#7759);
#6231=AXIS2_PLACEMENT_3D('',#9763,#7761,#7762);
#6232=AXIS2_PLACEMENT_3D('',#9764,#7763,#7764);
#7721=DIRECTION('axis',(0.,0.,1.));
#7722=DIRECTION('refdir',(1.,0.,0.));
#7723=DIRECTION('center_axis',(0.,-1.,0.));
#7724=DIRECTION('ref_axis',(0.,0.,-1.));
#7725=DIRECTION('center_axis',(0.,-1.,0.));
#7726=DIRECTION('ref_axis',(1.,0.,0.));
#7727=DIRECTION('center_axis',(0.,-1.,0.));
#7728=DIRECTION('ref_axis',(1.,0.,0.));
#7729=DIRECTION('center_axis',(1.,0.,1.22464679914735E-16));
#7730=DIRECTION('ref_axis',(-1.22464679914735E-16,0.,1.));
#7731=DIRECTION('center_axis',(0.,1.,0.));
#7732=DIRECTION('ref_axis',(1.,0.,0.));
#7733=DIRECTION('center_axis',(0.,1.,0.));
#7734=DIRECTION('ref_axis',(1.,0.,0.));
#7735=DIRECTION('center_axis',(0.,-1.,0.));
#7736=DIRECTION('ref_axis',(1.,0.,0.));
#7737=DIRECTION('center_axis',(0.,-1.,0.));
#7738=DIRECTION('ref_axis',(1.,0.,0.));
#7739=DIRECTION('',(0.,1.,0.));
#7740=DIRECTION('center_axis',(0.,1.,0.));
#7741=DIRECTION('ref_axis',(0.,0.,1.));
#7742=DIRECTION('center_axis',(0.,-1.,0.));
#7743=DIRECTION('ref_axis',(1.,0.,0.));
#7744=DIRECTION('center_axis',(0.,-1.,0.));
#7745=DIRECTION('ref_axis',(1.,0.,0.));
#7746=DIRECTION('center_axis',(0.,-1.,0.));
#7747=DIRECTION('ref_axis',(1.,0.,0.));
#7748=DIRECTION('center_axis',(0.,-1.,0.));
#7749=DIRECTION('ref_axis',(1.,0.,0.));
#7750=DIRECTION('',(0.707106781186548,0.707106781186547,8.65956056235494E-17));
#7751=DIRECTION('center_axis',(0.,-1.,0.));
#7752=DIRECTION('ref_axis',(1.,0.,0.));
#7753=DIRECTION('center_axis',(0.,-1.,0.));
#7754=DIRECTION('ref_axis',(1.,0.,0.));
#7755=DIRECTION('',(0.,1.,0.));
#7756=DIRECTION('center_axis',(0.,1.,0.));
#7757=DIRECTION('ref_axis',(1.,0.,0.));
#7758=DIRECTION('center_axis',(0.,-1.,0.));
#7759=DIRECTION('ref_axis',(1.,0.,0.));
#7760=DIRECTION('',(-0.707106781186548,0.707106781186547,-8.65956056235494E-17));
#7761=DIRECTION('center_axis',(0.,-1.,0.));
#7762=DIRECTION('ref_axis',(0.,0.,-1.));
#7763=DIRECTION('center_axis',(0.,-1.,0.));
#7764=DIRECTION('ref_axis',(1.,0.,0.));
#7765=DIRECTION('',(0.,1.,0.));
#9731=CARTESIAN_POINT('',(0.,0.,0.));
#9732=CARTESIAN_POINT('Origin',(0.,0.,0.));
#9733=CARTESIAN_POINT('',(-1.023815,0.246528389340863,-1.25381176266905E-16));
#9734=CARTESIAN_POINT('',(-1.25381176266905E-16,0.246528389340863,1.023815));
#9735=CARTESIAN_POINT('Origin',(0.,0.246528389340863,0.));
#9736=CARTESIAN_POINT('Origin',(0.,0.246528389340863,0.));
#9737=CARTESIAN_POINT('',(-1.25381176266905E-16,-0.246528389340863,1.023815));
#9738=CARTESIAN_POINT('Origin',(-1.22464679914735E-16,0.,1.));
#9739=CARTESIAN_POINT('',(-1.023815,-0.246528389340863,1.25381176266905E-16));
#9740=CARTESIAN_POINT('Origin',(0.,-0.246528389340863,0.));
#9741=CARTESIAN_POINT('Origin',(0.,-0.246528389340863,0.));
#9742=CARTESIAN_POINT('Origin',(0.,0.,0.));
#9743=CARTESIAN_POINT('',(-1.023815,-0.45,-1.25381176266905E-16));
#9744=CARTESIAN_POINT('Origin',(0.,-0.45,0.));
#9745=CARTESIAN_POINT('',(-1.023815,0.,-1.25381176266905E-16));
#9746=CARTESIAN_POINT('Origin',(1.44,0.45,0.));
#9747=CARTESIAN_POINT('',(-1.44,0.45,-1.76349139077219E-16));
#9748=CARTESIAN_POINT('Origin',(0.,0.45,0.));
#9749=CARTESIAN_POINT('',(-1.023815,0.45,-1.25381176266905E-16));
#9750=CARTESIAN_POINT('Origin',(0.,0.45,0.));
#9751=CARTESIAN_POINT('Origin',(0.,0.42,0.));
#9752=CARTESIAN_POINT('',(-1.5,0.39,-1.83697019872103E-16));
#9753=CARTESIAN_POINT('Origin',(0.,0.39,0.));
#9754=CARTESIAN_POINT('',(-1.47,0.42,-1.80023079474661E-16));
#9755=CARTESIAN_POINT('Origin',(0.,0.,0.));
#9756=CARTESIAN_POINT('',(-1.5,-0.39,-1.83697019872103E-16));
#9757=CARTESIAN_POINT('Origin',(0.,-0.39,0.));
#9758=CARTESIAN_POINT('',(-1.5,0.,-1.83697019872103E-16));
#9759=CARTESIAN_POINT('Origin',(0.,-0.42,0.));
#9760=CARTESIAN_POINT('',(-1.44,-0.45,-1.76349139077219E-16));
#9761=CARTESIAN_POINT('Origin',(0.,-0.45,0.));
#9762=CARTESIAN_POINT('',(-1.47,-0.42,-1.80023079474661E-16));
#9763=CARTESIAN_POINT('Origin',(1.023815,-0.45,0.));
#9764=CARTESIAN_POINT('Origin',(0.,0.,0.));
#9765=CARTESIAN_POINT('',(-1.023815,0.,-1.25381176266905E-16));
#10463=UNCERTAINTY_MEASURE_WITH_UNIT(LENGTH_MEASURE(0.001),#10511,
'DISTANCE_ACCURACY_VALUE',
'Maximum model space distance between geometric entities at asserted c
onnectivities');
#10471=UNCERTAINTY_MEASURE_WITH_UNIT(LENGTH_MEASURE(0.001),#10511,
'DISTANCE_ACCURACY_VALUE',
'Maximum model space distance between geometric entities at asserted c
onnectivities');
#10502=(
GEOMETRIC_REPRESENTATION_CONTEXT(3)
GLOBAL_UNCERTAINTY_ASSIGNED_CONTEXT((#10463))
GLOBAL_UNIT_ASSIGNED_CONTEXT((#10511,#10513,#10514))
REPRESENTATION_CONTEXT('','3D')
);
#10510=(
GEOMETRIC_REPRESENTATION_CONTEXT(3)
GLOBAL_UNCERTAINTY_ASSIGNED_CONTEXT((#10471))
GLOBAL_UNIT_ASSIGNED_CONTEXT((#10511,#10513,#10514))
REPRESENTATION_CONTEXT('','3D')
);
#10511=(
LENGTH_UNIT()
NAMED_UNIT(*)
SI_UNIT(.CENTI.,.METRE.)
);
#10513=(
NAMED_UNIT(*)
PLANE_ANGLE_UNIT()
SI_UNIT($,.RADIAN.)
);
#10514=(
NAMED_UNIT(*)
SI_UNIT($,.STERADIAN.)
SOLID_ANGLE_UNIT()
);
#10545=SHAPE_DEFINITION_REPRESENTATION(#10588,#10675);
#10588=PRODUCT_DEFINITION_SHAPE('',$,#10714);
#10675=SHAPE_REPRESENTATION('',(#6213),#10502);
#10683=PRODUCT_DEFINITION_CONTEXT('part definition',#10799,'design');
#10714=PRODUCT_DEFINITION('Outer ring (1)','Outer ring (1)',#10752,#10683);
#10752=PRODUCT_DEFINITION_FORMATION('',$,#10831);
#10799=APPLICATION_CONTEXT(
'Core Data for Automotive Mechanical Design Process');
#10800=PRODUCT_CONTEXT('part definition',#10799,'mechanical');
#10831=PRODUCT('Outer ring (1)','Outer ring (1)','Outer ring (1)',(#10800));
#10902=COLOUR_RGB('Grey',0.48,0.52,0.57);
#10903=FILL_AREA_STYLE_COLOUR('',#10902);
#10904=FILL_AREA_STYLE('',(#10903));
#10905=SURFACE_STYLE_FILL_AREA(#10904);
#10906=SURFACE_SIDE_STYLE('',(#10905));
#10907=SURFACE_STYLE_USAGE(.BOTH.,#10906);
#10908=PRESENTATION_STYLE_ASSIGNMENT((#10907));
ENDSEC;
END-ISO-10303-21;
